ISO-10303-21;
HEADER;
/* Generated by software containing ST-Developer
 * from STEP Tools, Inc. (www.steptools.com) 
 */

FILE_DESCRIPTION(
/* description */ ('Swing-away clamp arm'),
/* implementation_level */ '2;1');

FILE_NAME(
/* name */ 'M4x10 Cap Screw.step',
/* time_stamp */ '2026-10-28T03:26:03-07:00',
/* author */ (''),
/* organization */ (''),
/* preprocessor_version */ 'ST-DEVELOPER v20.2',
/* originating_system */ 'Autodesk Translation Framework v15.17.0.0',
/* authorisation */ '');

FILE_SCHEMA (('AUTOMOTIVE_DESIGN { 1 0 10303 214 3 1 1 }'));
ENDSEC;

DATA;
#10=MECHANICAL_DESIGN_GEOMETRIC_PRESENTATION_REPRESENTATION('',(#326),#10627);
#212=CONICAL_SURFACE('',#5831,0.325,0.785398163397448);
#213=CONICAL_SURFACE('',#5835,0.335,0.785398163397448);
#214=CONICAL_SURFACE('',#5839,0.21,0.463647609000806);
#217=ORIENTED_CLOSED_SHELL('',*,#4934,.F.);
#220=BREP_WITH_VOIDS('Body1',#4935,(#217));
#266=SHAPE_REPRESENTATION_RELATIONSHIP('SRR','None',#10767,#292);
#292=ADVANCED_BREP_SHAPE_REPRESENTATION('',(#220),#10626);
#326=STYLED_ITEM('',(#10972),#220);
#457=FACE_BOUND('',#1348,.T.);
#626=PLANE('',#5819);
#627=PLANE('',#5820);
#628=PLANE('',#5821);
#629=PLANE('',#5822);
#630=PLANE('',#5823);
#631=PLANE('',#5824);
#632=PLANE('',#5825);
#633=PLANE('',#5826);
#634=PLANE('',#5827);
#635=PLANE('',#5829);
#636=PLANE('',#5837);
#928=FACE_OUTER_BOUND('',#1334,.T.);
#929=FACE_OUTER_BOUND('',#1335,.T.);
#930=FACE_OUTER_BOUND('',#1336,.T.);
#931=FACE_OUTER_BOUND('',#1337,.T.);
#932=FACE_OUTER_BOUND('',#1338,.T.);
#933=FACE_OUTER_BOUND('',#1339,.T.);
#934=FACE_OUTER_BOUND('',#1340,.T.);
#935=FACE_OUTER_BOUND('',#1341,.T.);
#936=FACE_OUTER_BOUND('',#1342,.T.);
#937=FACE_OUTER_BOUND('',#1343,.T.);
#938=FACE_OUTER_BOUND('',#1344,.T.);
#939=FACE_OUTER_BOUND('',#1345,.T.);
#940=FACE_OUTER_BOUND('',#1346,.T.);
#941=FACE_OUTER_BOUND('',#1347,.T.);
#942=FACE_OUTER_BOUND('',#1349,.T.);
#943=FACE_OUTER_BOUND('',#1350,.T.);
#1334=EDGE_LOOP('',(#4437,#4438,#4439,#4440));
#1335=EDGE_LOOP('',(#4441,#4442,#4443,#4444));
#1336=EDGE_LOOP('',(#4445,#4446,#4447,#4448));
#1337=EDGE_LOOP('',(#4449,#4450,#4451,#4452));
#1338=EDGE_LOOP('',(#4453,#4454,#4455,#4456));
#1339=EDGE_LOOP('',(#4457,#4458,#4459,#4460));
#1340=EDGE_LOOP('',(#4461,#4462,#4463,#4464,#4465,#4466));
#1341=EDGE_LOOP('',(#4467,#4468,#4469,#4470,#4471,#4472));
#1342=EDGE_LOOP('',(#4473));
#1343=EDGE_LOOP('',(#4474));
#1344=EDGE_LOOP('',(#4475,#4476,#4477,#4478));
#1345=EDGE_LOOP('',(#4479,#4480,#4481,#4482));
#1346=EDGE_LOOP('',(#4483,#4484,#4485,#4486));
#1347=EDGE_LOOP('',(#4487));
#1348=EDGE_LOOP('',(#4488));
#1349=EDGE_LOOP('',(#4489,#4490,#4491,#4492));
#1350=EDGE_LOOP('',(#4493,#4494,#4495,#4496));
#1650=LINE('',#10474,#1972);
#1651=LINE('',#10476,#1973);
#1652=LINE('',#10478,#1974);
#1653=LINE('',#10479,#1975);
#1654=LINE('',#10482,#1976);
#1655=LINE('',#10484,#1977);
#1656=LINE('',#10485,#1978);
#1657=LINE('',#10488,#1979);
#1658=LINE('',#10490,#1980);
#1659=LINE('',#10491,#1981);
#1660=LINE('',#10494,#1982);
#1661=LINE('',#10496,#1983);
#1662=LINE('',#10497,#1984);
#1663=LINE('',#10500,#1985);
#1664=LINE('',#10502,#1986);
#1665=LINE('',#10503,#1987);
#1666=LINE('',#10505,#1988);
#1667=LINE('',#10506,#1989);
#1668=LINE('',#10518,#1990);
#1669=LINE('',#10522,#1991);
#1670=LINE('',#10526,#1992);
#1671=LINE('',#10533,#1993);
#1672=LINE('',#10535,#1994);
#1972=VECTOR('',#7363,1.);
#1973=VECTOR('',#7364,1.);
#1974=VECTOR('',#7365,1.);
#1975=VECTOR('',#7366,1.);
#1976=VECTOR('',#7369,1.);
#1977=VECTOR('',#7370,1.);
#1978=VECTOR('',#7371,1.);
#1979=VECTOR('',#7374,1.);
#1980=VECTOR('',#7375,1.);
#1981=VECTOR('',#7376,1.);
#1982=VECTOR('',#7379,1.);
#1983=VECTOR('',#7380,1.);
#1984=VECTOR('',#7381,1.);
#1985=VECTOR('',#7384,1.);
#1986=VECTOR('',#7385,1.);
#1987=VECTOR('',#7386,1.);
#1988=VECTOR('',#7389,1.);
#1989=VECTOR('',#7390,1.);
#1990=VECTOR('',#7407,0.325);
#1991=VECTOR('',#7412,0.35);
#1992=VECTOR('',#7417,0.335);
#1993=VECTOR('',#7426,0.21);
#1994=VECTOR('',#7429,0.2);
#2255=CIRCLE('',#5828,0.1954);
#2256=CIRCLE('',#5830,0.3);
#2257=CIRCLE('',#5832,0.35);
#2258=CIRCLE('',#5834,0.35);
#2259=CIRCLE('',#5836,0.32);
#2260=CIRCLE('',#5838,0.22);
#2261=CIRCLE('',#5840,0.1954);
#2654=VERTEX_POINT('',#10472);
#2655=VERTEX_POINT('',#10473);
#2656=VERTEX_POINT('',#10475);
#2657=VERTEX_POINT('',#10477);
#2658=VERTEX_POINT('',#10481);
#2659=VERTEX_POINT('',#10483);
#2660=VERTEX_POINT('',#10487);
#2661=VERTEX_POINT('',#10489);
#2662=VERTEX_POINT('',#10493);
#2663=VERTEX_POINT('',#10495);
#2664=VERTEX_POINT('',#10499);
#2665=VERTEX_POINT('',#10501);
#2666=VERTEX_POINT('',#10510);
#2667=VERTEX_POINT('',#10513);
#2668=VERTEX_POINT('',#10516);
#2669=VERTEX_POINT('',#10520);
#2670=VERTEX_POINT('',#10524);
#2671=VERTEX_POINT('',#10528);
#2672=VERTEX_POINT('',#10531);
#3251=EDGE_CURVE('',#2654,#2655,#1650,.T.);
#3252=EDGE_CURVE('',#2655,#2656,#1651,.T.);
#3253=EDGE_CURVE('',#2656,#2657,#1652,.T.);
#3254=EDGE_CURVE('',#2654,#2657,#1653,.T.);
#3255=EDGE_CURVE('',#2655,#2658,#1654,.T.);
#3256=EDGE_CURVE('',#2658,#2659,#1655,.T.);
#3257=EDGE_CURVE('',#2659,#2656,#1656,.T.);
#3258=EDGE_CURVE('',#2658,#2660,#1657,.T.);
#3259=EDGE_CURVE('',#2660,#2661,#1658,.T.);
#3260=EDGE_CURVE('',#2661,#2659,#1659,.T.);
#3261=EDGE_CURVE('',#2660,#2662,#1660,.T.);
#3262=EDGE_CURVE('',#2662,#2663,#1661,.T.);
#3263=EDGE_CURVE('',#2663,#2661,#1662,.T.);
#3264=EDGE_CURVE('',#2662,#2664,#1663,.T.);
#3265=EDGE_CURVE('',#2664,#2665,#1664,.T.);
#3266=EDGE_CURVE('',#2665,#2663,#1665,.T.);
#3267=EDGE_CURVE('',#2664,#2654,#1666,.T.);
#3268=EDGE_CURVE('',#2657,#2665,#1667,.T.);
#3269=EDGE_CURVE('',#2666,#2666,#2255,.T.);
#3270=EDGE_CURVE('',#2667,#2667,#2256,.T.);
#3271=EDGE_CURVE('',#2668,#2668,#2257,.T.);
#3272=EDGE_CURVE('',#2668,#2667,#1668,.T.);
#3273=EDGE_CURVE('',#2669,#2669,#2258,.T.);
#3274=EDGE_CURVE('',#2669,#2668,#1669,.T.);
#3275=EDGE_CURVE('',#2670,#2670,#2259,.T.);
#3276=EDGE_CURVE('',#2670,#2669,#1670,.T.);
#3277=EDGE_CURVE('',#2671,#2671,#2260,.T.);
#3278=EDGE_CURVE('',#2672,#2672,#2261,.F.);
#3279=EDGE_CURVE('',#2672,#2671,#1671,.T.);
#3280=EDGE_CURVE('',#2666,#2672,#1672,.T.);
#4437=ORIENTED_EDGE('',*,*,#3251,.T.);
#4438=ORIENTED_EDGE('',*,*,#3252,.T.);
#4439=ORIENTED_EDGE('',*,*,#3253,.T.);
#4440=ORIENTED_EDGE('',*,*,#3254,.F.);
#4441=ORIENTED_EDGE('',*,*,#3255,.T.);
#4442=ORIENTED_EDGE('',*,*,#3256,.T.);
#4443=ORIENTED_EDGE('',*,*,#3257,.T.);
#4444=ORIENTED_EDGE('',*,*,#3252,.F.);
#4445=ORIENTED_EDGE('',*,*,#3258,.T.);
#4446=ORIENTED_EDGE('',*,*,#3259,.T.);
#4447=ORIENTED_EDGE('',*,*,#3260,.T.);
#4448=ORIENTED_EDGE('',*,*,#3256,.F.);
#4449=ORIENTED_EDGE('',*,*,#3261,.T.);
#4450=ORIENTED_EDGE('',*,*,#3262,.T.);
#4451=ORIENTED_EDGE('',*,*,#3263,.T.);
#4452=ORIENTED_EDGE('',*,*,#3259,.F.);
#4453=ORIENTED_EDGE('',*,*,#3264,.T.);
#4454=ORIENTED_EDGE('',*,*,#3265,.T.);
#4455=ORIENTED_EDGE('',*,*,#3266,.T.);
#4456=ORIENTED_EDGE('',*,*,#3262,.F.);
#4457=ORIENTED_EDGE('',*,*,#3267,.T.);
#4458=ORIENTED_EDGE('',*,*,#3254,.T.);
#4459=ORIENTED_EDGE('',*,*,#3268,.T.);
#4460=ORIENTED_EDGE('',*,*,#3265,.F.);
#4461=ORIENTED_EDGE('',*,*,#3267,.F.);
#4462=ORIENTED_EDGE('',*,*,#3264,.F.);
#4463=ORIENTED_EDGE('',*,*,#3261,.F.);
#4464=ORIENTED_EDGE('',*,*,#3258,.F.);
#4465=ORIENTED_EDGE('',*,*,#3255,.F.);
#4466=ORIENTED_EDGE('',*,*,#3251,.F.);
#4467=ORIENTED_EDGE('',*,*,#3268,.F.);
#4468=ORIENTED_EDGE('',*,*,#3253,.F.);
#4469=ORIENTED_EDGE('',*,*,#3257,.F.);
#4470=ORIENTED_EDGE('',*,*,#3260,.F.);
#4471=ORIENTED_EDGE('',*,*,#3263,.F.);
#4472=ORIENTED_EDGE('',*,*,#3266,.F.);
#4473=ORIENTED_EDGE('',*,*,#3269,.F.);
#4474=ORIENTED_EDGE('',*,*,#3270,.F.);
#4475=ORIENTED_EDGE('',*,*,#3271,.F.);
#4476=ORIENTED_EDGE('',*,*,#3272,.T.);
#4477=ORIENTED_EDGE('',*,*,#3270,.T.);
#4478=ORIENTED_EDGE('',*,*,#3272,.F.);
#4479=ORIENTED_EDGE('',*,*,#3273,.F.);
#4480=ORIENTED_EDGE('',*,*,#3274,.T.);
#4481=ORIENTED_EDGE('',*,*,#3271,.T.);
#4482=ORIENTED_EDGE('',*,*,#3274,.F.);
#4483=ORIENTED_EDGE('',*,*,#3275,.F.);
#4484=ORIENTED_EDGE('',*,*,#3276,.T.);
#4485=ORIENTED_EDGE('',*,*,#3273,.T.);
#4486=ORIENTED_EDGE('',*,*,#3276,.F.);
#4487=ORIENTED_EDGE('',*,*,#3275,.T.);
#4488=ORIENTED_EDGE('',*,*,#3277,.F.);
#4489=ORIENTED_EDGE('',*,*,#3278,.F.);
#4490=ORIENTED_EDGE('',*,*,#3279,.T.);
#4491=ORIENTED_EDGE('',*,*,#3277,.T.);
#4492=ORIENTED_EDGE('',*,*,#3279,.F.);
#4493=ORIENTED_EDGE('',*,*,#3269,.T.);
#4494=ORIENTED_EDGE('',*,*,#3280,.T.);
#4495=ORIENTED_EDGE('',*,*,#3278,.T.);
#4496=ORIENTED_EDGE('',*,*,#3280,.F.);
#4590=CYLINDRICAL_SURFACE('',#5833,0.35);
#4591=CYLINDRICAL_SURFACE('',#5841,0.1954);
#4883=ADVANCED_FACE('',(#928),#626,.F.);
#4884=ADVANCED_FACE('',(#929),#627,.F.);
#4885=ADVANCED_FACE('',(#930),#628,.F.);
#4886=ADVANCED_FACE('',(#931),#629,.F.);
#4887=ADVANCED_FACE('',(#932),#630,.F.);
#4888=ADVANCED_FACE('',(#933),#631,.F.);
#4889=ADVANCED_FACE('',(#934),#632,.F.);
#4890=ADVANCED_FACE('',(#935),#633,.F.);
#4891=ADVANCED_FACE('',(#936),#634,.F.);
#4892=ADVANCED_FACE('',(#937),#635,.T.);
#4893=ADVANCED_FACE('',(#938),#212,.T.);
#4894=ADVANCED_FACE('',(#939),#4590,.T.);
#4895=ADVANCED_FACE('',(#940),#213,.T.);
#4896=ADVANCED_FACE('',(#941,#457),#636,.T.);
#4897=ADVANCED_FACE('',(#942),#214,.T.);
#4898=ADVANCED_FACE('',(#943),#4591,.T.);
#4934=CLOSED_SHELL('',(#4883,#4884,#4885,#4886,#4887,#4888,#4889,#4890));
#4935=CLOSED_SHELL('',(#4891,#4892,#4893,#4894,#4895,#4896,#4897,#4898));
#5818=AXIS2_PLACEMENT_3D('',#10470,#7359,#7360);
#5819=AXIS2_PLACEMENT_3D('',#10471,#7361,#7362);
#5820=AXIS2_PLACEMENT_3D('',#10480,#7367,#7368);
#5821=AXIS2_PLACEMENT_3D('',#10486,#7372,#7373);
#5822=AXIS2_PLACEMENT_3D('',#10492,#7377,#7378);
#5823=AXIS2_PLACEMENT_3D('',#10498,#7382,#7383);
#5824=AXIS2_PLACEMENT_3D('',#10504,#7387,#7388);
#5825=AXIS2_PLACEMENT_3D('',#10507,#7391,#7392);
#5826=AXIS2_PLACEMENT_3D('',#10508,#7393,#7394);
#5827=AXIS2_PLACEMENT_3D('',#10509,#7395,#7396);
#5828=AXIS2_PLACEMENT_3D('',#10511,#7397,#7398);
#5829=AXIS2_PLACEMENT_3D('',#10512,#7399,#7400);
#5830=AXIS2_PLACEMENT_3D('',#10514,#7401,#7402);
#5831=AXIS2_PLACEMENT_3D('',#10515,#7403,#7404);
#5832=AXIS2_PLACEMENT_3D('',#10517,#7405,#7406);
#5833=AXIS2_PLACEMENT_3D('',#10519,#7408,#7409);
#5834=AXIS2_PLACEMENT_3D('',#10521,#7410,#7411);
#5835=AXIS2_PLACEMENT_3D('',#10523,#7413,#7414);
#5836=AXIS2_PLACEMENT_3D('',#10525,#7415,#7416);
#5837=AXIS2_PLACEMENT_3D('',#10527,#7418,#7419);
#5838=AXIS2_PLACEMENT_3D('',#10529,#7420,#7421);
#5839=AXIS2_PLACEMENT_3D('',#10530,#7422,#7423);
#5840=AXIS2_PLACEMENT_3D('',#10532,#7424,#7425);
#5841=AXIS2_PLACEMENT_3D('',#10534,#7427,#7428);
#7359=DIRECTION('axis',(0.,0.,1.));
#7360=DIRECTION('refdir',(1.,0.,0.));
#7361=DIRECTION('center_axis',(0.866025403784439,0.,-0.5));
#7362=DIRECTION('ref_axis',(0.5,0.,0.866025403784439));
#7363=DIRECTION('',(-0.5,0.,-0.866025403784439));
#7364=DIRECTION('',(0.,-1.,0.));
#7365=DIRECTION('',(0.5,0.,0.866025403784439));
#7366=DIRECTION('',(0.,-1.,0.));
#7367=DIRECTION('center_axis',(1.60246890531964E-16,0.,-1.));
#7368=DIRECTION('ref_axis',(1.,0.,1.60246890531964E-16));
#7369=DIRECTION('',(-1.,0.,-1.60246890531964E-16));
#7370=DIRECTION('',(0.,-1.,0.));
#7371=DIRECTION('',(1.,0.,1.60246890531964E-16));
#7372=DIRECTION('center_axis',(-0.866025403784439,0.,-0.5));
#7373=DIRECTION('ref_axis',(0.5,0.,-0.866025403784439));
#7374=DIRECTION('',(-0.5,0.,0.866025403784439));
#7375=DIRECTION('',(0.,-1.,0.));
#7376=DIRECTION('',(0.5,0.,-0.866025403784439));
#7377=DIRECTION('center_axis',(-0.866025403784439,0.,0.5));
#7378=DIRECTION('ref_axis',(-0.5,0.,-0.866025403784439));
#7379=DIRECTION('',(0.5,0.,0.866025403784439));
#7380=DIRECTION('',(0.,-1.,0.));
#7381=DIRECTION('',(-0.5,0.,-0.866025403784439));
#7382=DIRECTION('center_axis',(-1.60246890531964E-16,0.,1.));
#7383=DIRECTION('ref_axis',(-1.,0.,-1.60246890531964E-16));
#7384=DIRECTION('',(1.,0.,1.60246890531964E-16));
#7385=DIRECTION('',(0.,-1.,0.));
#7386=DIRECTION('',(-1.,0.,-1.60246890531964E-16));
#7387=DIRECTION('center_axis',(0.866025403784439,0.,0.5));
#7388=DIRECTION('ref_axis',(-0.5,0.,0.866025403784439));
#7389=DIRECTION('',(0.5,0.,-0.866025403784439));
#7390=DIRECTION('',(-0.5,0.,0.866025403784439));
#7391=DIRECTION('center_axis',(0.,1.,0.));
#7392=DIRECTION('ref_axis',(1.,0.,0.));
#7393=DIRECTION('center_axis',(0.,-1.,0.));
#7394=DIRECTION('ref_axis',(0.,0.,-1.));
#7395=DIRECTION('center_axis',(0.,1.,0.));
#7396=DIRECTION('ref_axis',(1.,0.,0.));
#7397=DIRECTION('center_axis',(0.,1.,0.));
#7398=DIRECTION('ref_axis',(1.,0.,0.));
#7399=DIRECTION('center_axis',(0.,1.,0.));
#7400=DIRECTION('ref_axis',(0.,0.,1.));
#7401=DIRECTION('center_axis',(0.,-1.,0.));
#7402=DIRECTION('ref_axis',(1.,0.,0.));
#7403=DIRECTION('center_axis',(0.,-1.,0.));
#7404=DIRECTION('ref_axis',(1.,0.,0.));
#7405=DIRECTION('center_axis',(0.,-1.,0.));
#7406=DIRECTION('ref_axis',(1.,0.,0.));
#7407=DIRECTION('',(0.707106781186547,0.707106781186548,8.65956056235493E-17));
#7408=DIRECTION('center_axis',(0.,-1.,0.));
#7409=DIRECTION('ref_axis',(1.,0.,0.));
#7410=DIRECTION('center_axis',(0.,-1.,0.));
#7411=DIRECTION('ref_axis',(1.,0.,0.));
#7412=DIRECTION('',(0.,1.,0.));
#7413=DIRECTION('center_axis',(0.,1.,0.));
#7414=DIRECTION('ref_axis',(1.,0.,0.));
#7415=DIRECTION('center_axis',(0.,-1.,0.));
#7416=DIRECTION('ref_axis',(1.,0.,0.));
#7417=DIRECTION('',(-0.707106781186547,0.707106781186548,-8.65956056235493E-17));
#7418=DIRECTION('center_axis',(0.,-1.,0.));
#7419=DIRECTION('ref_axis',(0.,0.,-1.));
#7420=DIRECTION('center_axis',(0.,-1.,0.));
#7421=DIRECTION('ref_axis',(1.,0.,0.));
#7422=DIRECTION('center_axis',(0.,1.,0.));
#7423=DIRECTION('ref_axis',(1.,0.,0.));
#7424=DIRECTION('center_axis',(0.,1.,0.));
#7425=DIRECTION('ref_axis',(1.,0.,0.));
#7426=DIRECTION('',(-0.447213595499958,0.894427190999916,-5.47678698264203E-17));
#7427=DIRECTION('center_axis',(0.,-1.,0.));
#7428=DIRECTION('ref_axis',(1.,0.,0.));
#7429=DIRECTION('',(0.,1.,0.));
#10470=CARTESIAN_POINT('',(0.,0.,0.));
#10471=CARTESIAN_POINT('Origin',(0.0866025403784439,-0.4,-0.15));
#10472=CARTESIAN_POINT('',(0.173205080756888,-0.4,0.));
#10473=CARTESIAN_POINT('',(0.0866025403784439,-0.4,-0.15));
#10474=CARTESIAN_POINT('',(0.173205080756888,-0.4,0.));
#10475=CARTESIAN_POINT('',(0.0866025403784439,-0.64,-0.15));
#10476=CARTESIAN_POINT('',(0.0866025403784439,-0.4,-0.15));
#10477=CARTESIAN_POINT('',(0.173205080756888,-0.64,0.));
#10478=CARTESIAN_POINT('',(0.173205080756888,-0.64,0.));
#10479=CARTESIAN_POINT('',(0.173205080756888,-0.4,0.));
#10480=CARTESIAN_POINT('Origin',(-0.0866025403784438,-0.4,-0.15));
#10481=CARTESIAN_POINT('',(-0.0866025403784438,-0.4,-0.15));
#10482=CARTESIAN_POINT('',(0.0866025403784439,-0.4,-0.15));
#10483=CARTESIAN_POINT('',(-0.0866025403784438,-0.64,-0.15));
#10484=CARTESIAN_POINT('',(-0.0866025403784438,-0.4,-0.15));
#10485=CARTESIAN_POINT('',(0.0866025403784439,-0.64,-0.15));
#10486=CARTESIAN_POINT('Origin',(-0.173205080756888,-0.4,-2.77555756156289E-17));
#10487=CARTESIAN_POINT('',(-0.173205080756888,-0.4,-2.12115047744981E-17));
#10488=CARTESIAN_POINT('',(-0.0866025403784438,-0.4,-0.15));
#10489=CARTESIAN_POINT('',(-0.173205080756888,-0.64,-2.77555756156289E-17));
#10490=CARTESIAN_POINT('',(-0.173205080756888,-0.4,-2.12115047744981E-17));
#10491=CARTESIAN_POINT('',(-0.0866025403784438,-0.64,-0.15));
#10492=CARTESIAN_POINT('Origin',(-0.0866025403784439,-0.4,0.15));
#10493=CARTESIAN_POINT('',(-0.0866025403784439,-0.4,0.15));
#10494=CARTESIAN_POINT('',(-0.173205080756888,-0.4,-2.12115047744981E-17));
#10495=CARTESIAN_POINT('',(-0.0866025403784439,-0.64,0.15));
#10496=CARTESIAN_POINT('',(-0.0866025403784439,-0.4,0.15));
#10497=CARTESIAN_POINT('',(-0.173205080756888,-0.64,-2.12115047744981E-17));
#10498=CARTESIAN_POINT('Origin',(0.0866025403784439,-0.4,0.15));
#10499=CARTESIAN_POINT('',(0.0866025403784439,-0.4,0.15));
#10500=CARTESIAN_POINT('',(-0.0866025403784439,-0.4,0.15));
#10501=CARTESIAN_POINT('',(0.0866025403784439,-0.64,0.15));
#10502=CARTESIAN_POINT('',(0.0866025403784439,-0.4,0.15));
#10503=CARTESIAN_POINT('',(-0.0866025403784439,-0.64,0.15));
#10504=CARTESIAN_POINT('Origin',(0.173205080756888,-0.4,0.));
#10505=CARTESIAN_POINT('',(0.0866025403784439,-0.4,0.15));
#10506=CARTESIAN_POINT('',(0.0866025403784439,-0.64,0.15));
#10507=CARTESIAN_POINT('Origin',(0.,-0.4,-2.77555756156289E-17));
#10508=CARTESIAN_POINT('Origin',(0.,-0.64,-2.77555756156289E-17));
#10509=CARTESIAN_POINT('Origin',(0.,-1.,0.));
#10510=CARTESIAN_POINT('',(-0.1954,-1.,2.39295984553393E-17));
#10511=CARTESIAN_POINT('Origin',(0.,-1.,0.));
#10512=CARTESIAN_POINT('Origin',(0.3,0.4,0.));
#10513=CARTESIAN_POINT('',(-0.3,0.4,-3.67394039744206E-17));
#10514=CARTESIAN_POINT('Origin',(0.,0.4,0.));
#10515=CARTESIAN_POINT('Origin',(0.,0.375,0.));
#10516=CARTESIAN_POINT('',(-0.35,0.35,-4.28626379701573E-17));
#10517=CARTESIAN_POINT('Origin',(0.,0.35,0.));
#10518=CARTESIAN_POINT('',(-0.325,0.375,-3.9801020972289E-17));
#10519=CARTESIAN_POINT('Origin',(0.,0.19,0.));
#10520=CARTESIAN_POINT('',(-0.35,0.03,-4.28626379701574E-17));
#10521=CARTESIAN_POINT('Origin',(0.,0.03,0.));
#10522=CARTESIAN_POINT('',(-0.35,0.19,-4.28626379701574E-17));
#10523=CARTESIAN_POINT('Origin',(0.,0.0149999999999999,0.));
#10524=CARTESIAN_POINT('',(-0.32,-3.29597460435593E-17,-3.91886975727153E-17));
#10525=CARTESIAN_POINT('Origin',(0.,0.,0.));
#10526=CARTESIAN_POINT('',(-0.335,0.0149999999999999,-4.10256677714363E-17));
#10527=CARTESIAN_POINT('Origin',(0.22,0.,0.));
#10528=CARTESIAN_POINT('',(-0.22,-6.93889390390723E-18,-2.69422295812418E-17));
#10529=CARTESIAN_POINT('Origin',(0.,0.,0.));
#10530=CARTESIAN_POINT('Origin',(0.,-0.02,0.));
#10531=CARTESIAN_POINT('',(-0.1954,-0.0492,2.39295984553393E-17));
#10532=CARTESIAN_POINT('Origin',(0.,-0.0492,0.));
#10533=CARTESIAN_POINT('',(-0.21,-0.02,-2.57175827820944E-17));
#10534=CARTESIAN_POINT('Origin',(0.,-0.8,0.));
#10535=CARTESIAN_POINT('',(-0.1954,-0.8,-2.39295984553393E-17));
#10594=UNCERTAINTY_MEASURE_WITH_UNIT(LENGTH_MEASURE(0.001),#10628,
'DISTANCE_ACCURACY_VALUE',
'Maximum model space distance between geometric entities at asserted c
onnectivities');
#10595=UNCERTAINTY_MEASURE_WITH_UNIT(LENGTH_MEASURE(0.001),#10628,
'DISTANCE_ACCURACY_VALUE',
'Maximum model space distance between geometric entities at asserted c
onnectivities');
#10626=(
GEOMETRIC_REPRESENTATION_CONTEXT(3)
GLOBAL_UNCERTAINTY_ASSIGNED_CONTEXT((#10594))
GLOBAL_UNIT_ASSIGNED_CONTEXT((#10628,#10630,#10631))
REPRESENTATION_CONTEXT('','3D')
);
#10627=(
GEOMETRIC_REPRESENTATION_CONTEXT(3)
GLOBAL_UNCERTAINTY_ASSIGNED_CONTEXT((#10595))
GLOBAL_UNIT_ASSIGNED_CONTEXT((#10628,#10630,#10631))
REPRESENTATION_CONTEXT('','3D')
);
#10628=(
LENGTH_UNIT()
NAMED_UNIT(*)
SI_UNIT(.CENTI.,.METRE.)
);
#10630=(
NAMED_UNIT(*)
PLANE_ANGLE_UNIT()
SI_UNIT($,.RADIAN.)
);
#10631=(
NAMED_UNIT(*)
SI_UNIT($,.STERADIAN.)
SOLID_ANGLE_UNIT()
);
#10662=SHAPE_DEFINITION_REPRESENTATION(#10708,#10767);
#10708=PRODUCT_DEFINITION_SHAPE('',$,#10799);
#10767=SHAPE_REPRESENTATION('',(#5818),#10626);
#10768=PRODUCT_DEFINITION_CONTEXT('part definition',#10863,'design');
#10799=PRODUCT_DEFINITION('M4x10 Cap Screw','M4x10 Cap Screw',#10830,#10768);
#10830=PRODUCT_DEFINITION_FORMATION('',$,#10895);
#10863=APPLICATION_CONTEXT(
'Core Data for Automotive Mechanical Design Process');
#10864=PRODUCT_CONTEXT('part definition',#10863,'mechanical');
#10895=PRODUCT('M4x10 Cap Screw','M4x10 Cap Screw','M4x10 Cap Screw',(#10864));
#10966=COLOUR_RGB('Black',0.12,0.14,0.17);
#10967=FILL_AREA_STYLE_COLOUR('',#10966);
#10968=FILL_AREA_STYLE('',(#10967));
#10969=SURFACE_STYLE_FILL_AREA(#10968);
#10970=SURFACE_SIDE_STYLE('',(#10969));
#10971=SURFACE_STYLE_USAGE(.BOTH.,#10970);
#10972=PRESENTATION_STYLE_ASSIGNMENT((#10971));
ENDSEC;
END-ISO-10303-21;
